ISO-10303-21;
HEADER;
/* Generated by software containing ST-Developer
 * from STEP Tools, Inc. (www.steptools.com) 
 */

FILE_DESCRIPTION(
/* description */ (''),
/* implementation_level */ '2;1');

FILE_NAME(
/* name */ 'M3_Screw_02 (1).step',
/* time_stamp */ '2026-10-22T15:07:41+06:00',
/* author */ (''),
/* organization */ (''),
/* preprocessor_version */ 'ST-DEVELOPER v20.2',
/* originating_system */ 'Autodesk Translation Framework v15.15.0.0',
/* authorisation */ '');

FILE_SCHEMA (('AUTOMOTIVE_DESIGN { 1 0 10303 214 3 1 1 }'));
ENDSEC;

DATA;
#10=MECHANICAL_DESIGN_GEOMETRIC_PRESENTATION_REPRESENTATION('',(#2887),#19220);
#76=SHAPE_REPRESENTATION_RELATIONSHIP('SRR','None',#19279,#90);
#90=ADVANCED_BREP_SHAPE_REPRESENTATION('',(#104),#19215);
#104=MANIFOLD_SOLID_BREP('M3_Screw_02',#11323);
#617=FACE_BOUND('',#4414,.T.);
#780=PLANE('',#12591);
#781=PLANE('',#12593);
#782=PLANE('',#12594);
#783=PLANE('',#12595);
#784=PLANE('',#12596);
#785=PLANE('',#12597);
#786=PLANE('',#12598);
#787=PLANE('',#12599);
#788=PLANE('',#12602);
#1530=LINE('',#18755,#2385);
#1531=LINE('',#18757,#2386);
#1532=LINE('',#18759,#2387);
#1533=LINE('',#18761,#2388);
#1534=LINE('',#18763,#2389);
#1535=LINE('',#18764,#2390);
#1536=LINE('',#18769,#2391);
#1537=LINE('',#18771,#2392);
#1538=LINE('',#18772,#2393);
#1539=LINE('',#18775,#2394);
#1540=LINE('',#18776,#2395);
#1541=LINE('',#18779,#2396);
#1542=LINE('',#18780,#2397);
#1543=LINE('',#18783,#2398);
#1544=LINE('',#18784,#2399);
#1545=LINE('',#18787,#2400);
#1546=LINE('',#18788,#2401);
#1547=LINE('',#18790,#2402);
#1548=LINE('',#18795,#2403);
#2385=VECTOR('',#15637,10.);
#2386=VECTOR('',#15638,10.);
#2387=VECTOR('',#15639,10.);
#2388=VECTOR('',#15640,10.);
#2389=VECTOR('',#15641,10.);
#2390=VECTOR('',#15642,10.);
#2391=VECTOR('',#15647,10.);
#2392=VECTOR('',#15648,10.);
#2393=VECTOR('',#15649,10.);
#2394=VECTOR('',#15652,10.);
#2395=VECTOR('',#15653,10.);
#2396=VECTOR('',#15656,10.);
#2397=VECTOR('',#15657,10.);
#2398=VECTOR('',#15660,10.);
#2399=VECTOR('',#15661,10.);
#2400=VECTOR('',#15664,10.);
#2401=VECTOR('',#15665,10.);
#2402=VECTOR('',#15668,10.);
#2403=VECTOR('',#15675,1.49999999999999);
#2856=CYLINDRICAL_SURFACE('',#12600,1.4635);
#2887=STYLED_ITEM('',(#19410),#104);
#3359=FACE_OUTER_BOUND('',#4413,.T.);
#3360=FACE_OUTER_BOUND('',#4415,.T.);
#3361=FACE_OUTER_BOUND('',#4416,.T.);
#3362=FACE_OUTER_BOUND('',#4417,.T.);
#3363=FACE_OUTER_BOUND('',#4418,.T.);
#3364=FACE_OUTER_BOUND('',#4419,.T.);
#3365=FACE_OUTER_BOUND('',#4420,.T.);
#3366=FACE_OUTER_BOUND('',#4421,.T.);
#3367=FACE_OUTER_BOUND('',#4422,.T.);
#3368=FACE_OUTER_BOUND('',#4423,.T.);
#4413=EDGE_LOOP('',(#10354,#10355,#10356,#10357,#10358,#10359));
#4414=EDGE_LOOP('',(#10360));
#4415=EDGE_LOOP('',(#10361,#10362,#10363,#10364));
#4416=EDGE_LOOP('',(#10365,#10366,#10367,#10368));
#4417=EDGE_LOOP('',(#10369,#10370,#10371,#10372));
#4418=EDGE_LOOP('',(#10373,#10374,#10375,#10376));
#4419=EDGE_LOOP('',(#10377,#10378,#10379,#10380));
#4420=EDGE_LOOP('',(#10381,#10382,#10383,#10384));
#4421=EDGE_LOOP('',(#10385,#10386,#10387,#10388,#10389,#10390));
#4422=EDGE_LOOP('',(#10391,#10392,#10393,#10394));
#4423=EDGE_LOOP('',(#10395));
#5131=CIRCLE('',#12592,1.4635);
#5132=CIRCLE('',#12601,1.4635);
#6051=VERTEX_POINT('',#18753);
#6052=VERTEX_POINT('',#18754);
#6053=VERTEX_POINT('',#18756);
#6054=VERTEX_POINT('',#18758);
#6055=VERTEX_POINT('',#18760);
#6056=VERTEX_POINT('',#18762);
#6057=VERTEX_POINT('',#18765);
#6058=VERTEX_POINT('',#18768);
#6059=VERTEX_POINT('',#18770);
#6060=VERTEX_POINT('',#18774);
#6061=VERTEX_POINT('',#18778);
#6062=VERTEX_POINT('',#18782);
#6063=VERTEX_POINT('',#18786);
#6064=VERTEX_POINT('',#18793);
#7508=EDGE_CURVE('',#6051,#6052,#1530,.T.);
#7509=EDGE_CURVE('',#6053,#6051,#1531,.T.);
#7510=EDGE_CURVE('',#6054,#6053,#1532,.T.);
#7511=EDGE_CURVE('',#6055,#6054,#1533,.T.);
#7512=EDGE_CURVE('',#6056,#6055,#1534,.T.);
#7513=EDGE_CURVE('',#6052,#6056,#1535,.T.);
#7514=EDGE_CURVE('',#6057,#6057,#5131,.F.);
#7515=EDGE_CURVE('',#6051,#6058,#1536,.T.);
#7516=EDGE_CURVE('',#6059,#6058,#1537,.T.);
#7517=EDGE_CURVE('',#6053,#6059,#1538,.T.);
#7518=EDGE_CURVE('',#6060,#6059,#1539,.T.);
#7519=EDGE_CURVE('',#6054,#6060,#1540,.T.);
#7520=EDGE_CURVE('',#6061,#6060,#1541,.T.);
#7521=EDGE_CURVE('',#6055,#6061,#1542,.T.);
#7522=EDGE_CURVE('',#6062,#6061,#1543,.T.);
#7523=EDGE_CURVE('',#6056,#6062,#1544,.T.);
#7524=EDGE_CURVE('',#6063,#6062,#1545,.T.);
#7525=EDGE_CURVE('',#6052,#6063,#1546,.T.);
#7526=EDGE_CURVE('',#6058,#6063,#1547,.T.);
#7527=EDGE_CURVE('',#6064,#6064,#5132,.T.);
#7528=EDGE_CURVE('',#6064,#6057,#1548,.T.);
#10354=ORIENTED_EDGE('',*,*,#7508,.F.);
#10355=ORIENTED_EDGE('',*,*,#7509,.F.);
#10356=ORIENTED_EDGE('',*,*,#7510,.F.);
#10357=ORIENTED_EDGE('',*,*,#7511,.F.);
#10358=ORIENTED_EDGE('',*,*,#7512,.F.);
#10359=ORIENTED_EDGE('',*,*,#7513,.F.);
#10360=ORIENTED_EDGE('',*,*,#7514,.T.);
#10361=ORIENTED_EDGE('',*,*,#7509,.T.);
#10362=ORIENTED_EDGE('',*,*,#7515,.T.);
#10363=ORIENTED_EDGE('',*,*,#7516,.F.);
#10364=ORIENTED_EDGE('',*,*,#7517,.F.);
#10365=ORIENTED_EDGE('',*,*,#7510,.T.);
#10366=ORIENTED_EDGE('',*,*,#7517,.T.);
#10367=ORIENTED_EDGE('',*,*,#7518,.F.);
#10368=ORIENTED_EDGE('',*,*,#7519,.F.);
#10369=ORIENTED_EDGE('',*,*,#7511,.T.);
#10370=ORIENTED_EDGE('',*,*,#7519,.T.);
#10371=ORIENTED_EDGE('',*,*,#7520,.F.);
#10372=ORIENTED_EDGE('',*,*,#7521,.F.);
#10373=ORIENTED_EDGE('',*,*,#7512,.T.);
#10374=ORIENTED_EDGE('',*,*,#7521,.T.);
#10375=ORIENTED_EDGE('',*,*,#7522,.F.);
#10376=ORIENTED_EDGE('',*,*,#7523,.F.);
#10377=ORIENTED_EDGE('',*,*,#7513,.T.);
#10378=ORIENTED_EDGE('',*,*,#7523,.T.);
#10379=ORIENTED_EDGE('',*,*,#7524,.F.);
#10380=ORIENTED_EDGE('',*,*,#7525,.F.);
#10381=ORIENTED_EDGE('',*,*,#7508,.T.);
#10382=ORIENTED_EDGE('',*,*,#7525,.T.);
#10383=ORIENTED_EDGE('',*,*,#7526,.F.);
#10384=ORIENTED_EDGE('',*,*,#7515,.F.);
#10385=ORIENTED_EDGE('',*,*,#7526,.T.);
#10386=ORIENTED_EDGE('',*,*,#7524,.T.);
#10387=ORIENTED_EDGE('',*,*,#7522,.T.);
#10388=ORIENTED_EDGE('',*,*,#7520,.T.);
#10389=ORIENTED_EDGE('',*,*,#7518,.T.);
#10390=ORIENTED_EDGE('',*,*,#7516,.T.);
#10391=ORIENTED_EDGE('',*,*,#7527,.F.);
#10392=ORIENTED_EDGE('',*,*,#7528,.T.);
#10393=ORIENTED_EDGE('',*,*,#7514,.F.);
#10394=ORIENTED_EDGE('',*,*,#7528,.F.);
#10395=ORIENTED_EDGE('',*,*,#7527,.T.);
#11235=ADVANCED_FACE('',(#3359,#617),#780,.F.);
#11236=ADVANCED_FACE('',(#3360),#781,.T.);
#11237=ADVANCED_FACE('',(#3361),#782,.T.);
#11238=ADVANCED_FACE('',(#3362),#783,.T.);
#11239=ADVANCED_FACE('',(#3363),#784,.T.);
#11240=ADVANCED_FACE('',(#3364),#785,.T.);
#11241=ADVANCED_FACE('',(#3365),#786,.T.);
#11242=ADVANCED_FACE('',(#3366),#787,.T.);
#11243=ADVANCED_FACE('',(#3367),#2856,.T.);
#11244=ADVANCED_FACE('',(#3368),#788,.F.);
#11323=CLOSED_SHELL('',(#11235,#11236,#11237,#11238,#11239,#11240,#11241,
#11242,#11243,#11244));
#12590=AXIS2_PLACEMENT_3D('',#18751,#15633,#15634);
#12591=AXIS2_PLACEMENT_3D('',#18752,#15635,#15636);
#12592=AXIS2_PLACEMENT_3D('',#18766,#15643,#15644);
#12593=AXIS2_PLACEMENT_3D('',#18767,#15645,#15646);
#12594=AXIS2_PLACEMENT_3D('',#18773,#15650,#15651);
#12595=AXIS2_PLACEMENT_3D('',#18777,#15654,#15655);
#12596=AXIS2_PLACEMENT_3D('',#18781,#15658,#15659);
#12597=AXIS2_PLACEMENT_3D('',#18785,#15662,#15663);
#12598=AXIS2_PLACEMENT_3D('',#18789,#15666,#15667);
#12599=AXIS2_PLACEMENT_3D('',#18791,#15669,#15670);
#12600=AXIS2_PLACEMENT_3D('',#18792,#15671,#15672);
#12601=AXIS2_PLACEMENT_3D('',#18794,#15673,#15674);
#12602=AXIS2_PLACEMENT_3D('',#18796,#15676,#15677);
#15633=DIRECTION('axis',(0.,0.,1.));
#15634=DIRECTION('refdir',(1.,0.,0.));
#15635=DIRECTION('center_axis',(0.,-1.,0.));
#15636=DIRECTION('ref_axis',(1.,0.,0.));
#15637=DIRECTION('',(0.427641188232285,0.,0.903948568297599));
#15638=DIRECTION('',(0.996663017976436,0.,0.0816261514350802));
#15639=DIRECTION('',(0.569021829744153,0.,-0.82232241686252));
#15640=DIRECTION('',(-0.427641188232283,0.,-0.9039485682976));
#15641=DIRECTION('',(-0.996663017976436,0.,-0.0816261514350783));
#15642=DIRECTION('',(-0.569021829744152,0.,0.822322416862521));
#15643=DIRECTION('center_axis',(0.,1.,0.));
#15644=DIRECTION('ref_axis',(1.,0.,0.));
#15645=DIRECTION('center_axis',(0.0816261514350802,0.,-0.996663017976436));
#15646=DIRECTION('ref_axis',(0.996663017976436,0.,0.0816261514350802));
#15647=DIRECTION('',(0.,-1.,0.));
#15648=DIRECTION('',(0.996663017976436,0.,0.0816261514350802));
#15649=DIRECTION('',(0.,-1.,0.));
#15650=DIRECTION('center_axis',(-0.82232241686252,0.,-0.569021829744153));
#15651=DIRECTION('ref_axis',(0.569021829744153,0.,-0.82232241686252));
#15652=DIRECTION('',(0.569021829744153,0.,-0.82232241686252));
#15653=DIRECTION('',(0.,-1.,0.));
#15654=DIRECTION('center_axis',(-0.9039485682976,0.,0.427641188232283));
#15655=DIRECTION('ref_axis',(-0.427641188232283,0.,-0.9039485682976));
#15656=DIRECTION('',(-0.427641188232283,0.,-0.9039485682976));
#15657=DIRECTION('',(0.,-1.,0.));
#15658=DIRECTION('center_axis',(-0.0816261514350783,0.,0.996663017976436));
#15659=DIRECTION('ref_axis',(-0.996663017976436,0.,-0.0816261514350783));
#15660=DIRECTION('',(-0.996663017976436,0.,-0.0816261514350783));
#15661=DIRECTION('',(0.,-1.,0.));
#15662=DIRECTION('center_axis',(0.822322416862521,0.,0.569021829744152));
#15663=DIRECTION('ref_axis',(-0.569021829744152,0.,0.822322416862521));
#15664=DIRECTION('',(-0.569021829744152,0.,0.822322416862521));
#15665=DIRECTION('',(0.,-1.,0.));
#15666=DIRECTION('center_axis',(0.903948568297599,0.,-0.427641188232285));
#15667=DIRECTION('ref_axis',(0.427641188232285,0.,0.903948568297599));
#15668=DIRECTION('',(0.427641188232285,0.,0.903948568297599));
#15669=DIRECTION('center_axis',(0.,-1.,0.));
#15670=DIRECTION('ref_axis',(1.,0.,0.));
#15671=DIRECTION('center_axis',(0.,1.,0.));
#15672=DIRECTION('ref_axis',(1.,0.,0.));
#15673=DIRECTION('center_axis',(0.,1.,0.));
#15674=DIRECTION('ref_axis',(1.,0.,0.));
#15675=DIRECTION('',(0.,-1.,0.));
#15676=DIRECTION('center_axis',(0.,-1.,0.));
#15677=DIRECTION('ref_axis',(1.,0.,0.));
#18751=CARTESIAN_POINT('',(0.,0.,0.));
#18752=CARTESIAN_POINT('Origin',(67.9877341799264,50.,25.7372649179816));
#18753=CARTESIAN_POINT('',(69.3018338062367,50.,23.8381926430366));
#18754=CARTESIAN_POINT('',(70.2894288268066,50.,25.9257724399974));
#18755=CARTESIAN_POINT('',(69.3018338062367,50.,23.8381926430366));
#18756=CARTESIAN_POINT('',(67.0001391593565,50.,23.6496851210208));
#18757=CARTESIAN_POINT('',(67.0001391593565,50.,23.6496851210208));
#18758=CARTESIAN_POINT('',(65.6860395330462,50.,25.5487573959657));
#18759=CARTESIAN_POINT('',(65.6860395330462,50.,25.5487573959657));
#18760=CARTESIAN_POINT('',(66.6736345536162,50.,27.6363371929265));
#18761=CARTESIAN_POINT('',(66.6736345536162,50.,27.6363371929265));
#18762=CARTESIAN_POINT('',(68.9753292004963,50.,27.8248447149424));
#18763=CARTESIAN_POINT('',(68.9753292004963,50.,27.8248447149424));
#18764=CARTESIAN_POINT('',(70.2894288268066,50.,25.9257724399974));
#18765=CARTESIAN_POINT('',(66.5242341799264,50.,25.7372649179816));
#18766=CARTESIAN_POINT('Origin',(67.9877341799264,50.,25.7372649179816));
#18767=CARTESIAN_POINT('Origin',(67.0001391593565,50.,23.6496851210208));
#18768=CARTESIAN_POINT('',(69.3018338062367,49.,23.8381926430366));
#18769=CARTESIAN_POINT('',(69.3018338062367,50.,23.8381926430366));
#18770=CARTESIAN_POINT('',(67.0001391593565,49.,23.6496851210208));
#18771=CARTESIAN_POINT('',(67.0001391593565,49.,23.6496851210208));
#18772=CARTESIAN_POINT('',(67.0001391593565,50.,23.6496851210208));
#18773=CARTESIAN_POINT('Origin',(65.6860395330462,50.,25.5487573959657));
#18774=CARTESIAN_POINT('',(65.6860395330462,49.,25.5487573959657));
#18775=CARTESIAN_POINT('',(65.6860395330462,49.,25.5487573959657));
#18776=CARTESIAN_POINT('',(65.6860395330462,50.,25.5487573959657));
#18777=CARTESIAN_POINT('Origin',(66.6736345536162,50.,27.6363371929265));
#18778=CARTESIAN_POINT('',(66.6736345536162,49.,27.6363371929265));
#18779=CARTESIAN_POINT('',(66.6736345536162,49.,27.6363371929265));
#18780=CARTESIAN_POINT('',(66.6736345536162,50.,27.6363371929265));
#18781=CARTESIAN_POINT('Origin',(68.9753292004963,50.,27.8248447149424));
#18782=CARTESIAN_POINT('',(68.9753292004963,49.,27.8248447149424));
#18783=CARTESIAN_POINT('',(68.9753292004963,49.,27.8248447149424));
#18784=CARTESIAN_POINT('',(68.9753292004963,50.,27.8248447149424));
#18785=CARTESIAN_POINT('Origin',(70.2894288268066,50.,25.9257724399974));
#18786=CARTESIAN_POINT('',(70.2894288268066,49.,25.9257724399974));
#18787=CARTESIAN_POINT('',(70.2894288268066,49.,25.9257724399974));
#18788=CARTESIAN_POINT('',(70.2894288268066,50.,25.9257724399974));
#18789=CARTESIAN_POINT('Origin',(69.3018338062367,50.,23.8381926430366));
#18790=CARTESIAN_POINT('',(69.3018338062367,49.,23.8381926430366));
#18791=CARTESIAN_POINT('Origin',(67.9877341799264,49.,25.7372649179816));
#18792=CARTESIAN_POINT('Origin',(67.9877341799264,50.,25.7372649179816));
#18793=CARTESIAN_POINT('',(66.5242341799264,63.,25.7372649179816));
#18794=CARTESIAN_POINT('Origin',(67.9877341799264,63.,25.7372649179816));
#18795=CARTESIAN_POINT('',(66.5242341799264,50.,25.7372649179816));
#18796=CARTESIAN_POINT('Origin',(67.9877341799264,63.,25.7372649179816));
#19199=UNCERTAINTY_MEASURE_WITH_UNIT(LENGTH_MEASURE(0.01),#19221,
'DISTANCE_ACCURACY_VALUE',
'Maximum model space distance between geometric entities at asserted c
onnectivities');
#19204=UNCERTAINTY_MEASURE_WITH_UNIT(LENGTH_MEASURE(0.01),#19221,
'DISTANCE_ACCURACY_VALUE',
'Maximum model space distance between geometric entities at asserted c
onnectivities');
#19215=(
GEOMETRIC_REPRESENTATION_CONTEXT(3)
GLOBAL_UNCERTAINTY_ASSIGNED_CONTEXT((#19199))
GLOBAL_UNIT_ASSIGNED_CONTEXT((#19221,#19223,#19224))
REPRESENTATION_CONTEXT('','3D')
);
#19220=(
GEOMETRIC_REPRESENTATION_CONTEXT(3)
GLOBAL_UNCERTAINTY_ASSIGNED_CONTEXT((#19204))
GLOBAL_UNIT_ASSIGNED_CONTEXT((#19221,#19223,#19224))
REPRESENTATION_CONTEXT('','3D')
);
#19221=(
LENGTH_UNIT()
NAMED_UNIT(*)
SI_UNIT(.MILLI.,.METRE.)
);
#19223=(
NAMED_UNIT(*)
PLANE_ANGLE_UNIT()
SI_UNIT($,.RADIAN.)
);
#19224=(
NAMED_UNIT(*)
SI_UNIT($,.STERADIAN.)
SOLID_ANGLE_UNIT()
);
#19235=SHAPE_DEFINITION_REPRESENTATION(#19250,#19279);
#19250=PRODUCT_DEFINITION_SHAPE('',$,#19295);
#19279=SHAPE_REPRESENTATION('',(#12590),#19215);
#19284=PRODUCT_DEFINITION_CONTEXT('part definition',#19331,'design');
#19295=PRODUCT_DEFINITION('M3_Screw_02 (1)','M3_Screw_02 (1)',#19310,#19284);
#19310=PRODUCT_DEFINITION_FORMATION('',$,#19343);
#19331=APPLICATION_CONTEXT(
'Core Data for Automotive Mechanical Design Process');
#19332=PRODUCT_CONTEXT('part definition',#19331,'mechanical');
#19343=PRODUCT('M3_Screw_02 (1)','M3_Screw_02 (1)',$,(#19332));
#19404=COLOUR_RGB('Black',0.12,0.14,0.17);
#19405=FILL_AREA_STYLE_COLOUR('',#19404);
#19406=FILL_AREA_STYLE('',(#19405));
#19407=SURFACE_STYLE_FILL_AREA(#19406);
#19408=SURFACE_SIDE_STYLE('',(#19407));
#19409=SURFACE_STYLE_USAGE(.BOTH.,#19408);
#19410=PRESENTATION_STYLE_ASSIGNMENT((#19409));
ENDSEC;
END-ISO-10303-21;
